ISO-10303-21;
HEADER;
/* Generated by software containing ST-Developer
 * from STEP Tools, Inc. (www.steptools.com) 
 */

FILE_DESCRIPTION(
/* description */ ('Four-valve pipe header'),
/* implementation_level */ '2;1');

FILE_NAME(
/* name */ 'M5x70 body screw.step',
/* time_stamp */ '2026-10-29T16:56:19-07:00',
/* author */ (''),
/* organization */ (''),
/* preprocessor_version */ 'ST-DEVELOPER v20.2',
/* originating_system */ 'Autodesk Translation Framework v15.17.0.0',
/* authorisation */ '');

FILE_SCHEMA (('AUTOMOTIVE_DESIGN { 1 0 10303 214 3 1 1 }'));
ENDSEC;

DATA;
#10=MECHANICAL_DESIGN_GEOMETRIC_PRESENTATION_REPRESENTATION('',(#346),#10119);
#235=ORIENTED_CLOSED_SHELL('',*,#5592,.F.);
#238=BREP_WITH_VOIDS('Body1',#5593,(#235));
#266=CONICAL_SURFACE('',#6307,0.4,0.785398163397448);
#267=CONICAL_SURFACE('',#6311,0.41,0.785398163397448);
#268=CONICAL_SURFACE('',#6315,0.26,0.463647609000806);
#294=SHAPE_REPRESENTATION_RELATIONSHIP('SRR','None',#10256,#320);
#320=ADVANCED_BREP_SHAPE_REPRESENTATION('',(#238),#10105);
#346=STYLED_ITEM('',(#10477),#238);
#513=FACE_BOUND('',#1369,.T.);
#514=FACE_BOUND('',#1377,.T.);
#646=PLANE('',#6291);
#647=PLANE('',#6292);
#648=PLANE('',#6293);
#649=PLANE('',#6294);
#650=PLANE('',#6295);
#651=PLANE('',#6296);
#652=PLANE('',#6297);
#653=PLANE('',#6298);
#654=PLANE('',#6299);
#655=PLANE('',#6304);
#656=PLANE('',#6305);
#657=PLANE('',#6313);
#941=FACE_OUTER_BOUND('',#1360,.T.);
#942=FACE_OUTER_BOUND('',#1361,.T.);
#943=FACE_OUTER_BOUND('',#1362,.T.);
#944=FACE_OUTER_BOUND('',#1363,.T.);
#945=FACE_OUTER_BOUND('',#1364,.T.);
#946=FACE_OUTER_BOUND('',#1365,.T.);
#947=FACE_OUTER_BOUND('',#1366,.T.);
#948=FACE_OUTER_BOUND('',#1367,.T.);
#949=FACE_OUTER_BOUND('',#1368,.T.);
#950=FACE_OUTER_BOUND('',#1370,.T.);
#951=FACE_OUTER_BOUND('',#1371,.T.);
#952=FACE_OUTER_BOUND('',#1372,.T.);
#953=FACE_OUTER_BOUND('',#1373,.T.);
#954=FACE_OUTER_BOUND('',#1374,.T.);
#955=FACE_OUTER_BOUND('',#1375,.T.);
#956=FACE_OUTER_BOUND('',#1376,.T.);
#957=FACE_OUTER_BOUND('',#1378,.T.);
#958=FACE_OUTER_BOUND('',#1379,.T.);
#1360=EDGE_LOOP('',(#4603,#4604,#4605,#4606));
#1361=EDGE_LOOP('',(#4607,#4608,#4609,#4610));
#1362=EDGE_LOOP('',(#4611,#4612,#4613,#4614));
#1363=EDGE_LOOP('',(#4615,#4616,#4617,#4618));
#1364=EDGE_LOOP('',(#4619,#4620,#4621,#4622));
#1365=EDGE_LOOP('',(#4623,#4624,#4625,#4626));
#1366=EDGE_LOOP('',(#4627,#4628,#4629,#4630,#4631,#4632));
#1367=EDGE_LOOP('',(#4633,#4634,#4635,#4636,#4637,#4638));
#1368=EDGE_LOOP('',(#4639));
#1369=EDGE_LOOP('',(#4640));
#1370=EDGE_LOOP('',(#4641,#4642,#4643,#4644));
#1371=EDGE_LOOP('',(#4645));
#1372=EDGE_LOOP('',(#4646));
#1373=EDGE_LOOP('',(#4647,#4648,#4649,#4650));
#1374=EDGE_LOOP('',(#4651,#4652,#4653,#4654));
#1375=EDGE_LOOP('',(#4655,#4656,#4657,#4658));
#1376=EDGE_LOOP('',(#4659));
#1377=EDGE_LOOP('',(#4660));
#1378=EDGE_LOOP('',(#4661,#4662,#4663,#4664));
#1379=EDGE_LOOP('',(#4665,#4666,#4667,#4668));
#1748=LINE('',#9382,#2166);
#1749=LINE('',#9384,#2167);
#1750=LINE('',#9386,#2168);
#1751=LINE('',#9387,#2169);
#1752=LINE('',#9390,#2170);
#1753=LINE('',#9392,#2171);
#1754=LINE('',#9393,#2172);
#1755=LINE('',#9396,#2173);
#1756=LINE('',#9398,#2174);
#1757=LINE('',#9399,#2175);
#1758=LINE('',#9402,#2176);
#1759=LINE('',#9404,#2177);
#1760=LINE('',#9405,#2178);
#1761=LINE('',#9408,#2179);
#1762=LINE('',#9410,#2180);
#1763=LINE('',#9411,#2181);
#1764=LINE('',#9413,#2182);
#1765=LINE('',#9414,#2183);
#1766=LINE('',#9424,#2184);
#1767=LINE('',#9433,#2185);
#1768=LINE('',#9437,#2186);
#1769=LINE('',#9441,#2187);
#1770=LINE('',#9448,#2188);
#1771=LINE('',#9450,#2189);
#2166=VECTOR('',#7591,1.);
#2167=VECTOR('',#7592,1.);
#2168=VECTOR('',#7593,1.);
#2169=VECTOR('',#7594,1.);
#2170=VECTOR('',#7597,1.);
#2171=VECTOR('',#7598,1.);
#2172=VECTOR('',#7599,1.);
#2173=VECTOR('',#7602,1.);
#2174=VECTOR('',#7603,1.);
#2175=VECTOR('',#7604,1.);
#2176=VECTOR('',#7607,1.);
#2177=VECTOR('',#7608,1.);
#2178=VECTOR('',#7609,1.);
#2179=VECTOR('',#7612,1.);
#2180=VECTOR('',#7613,1.);
#2181=VECTOR('',#7614,1.);
#2182=VECTOR('',#7617,1.);
#2183=VECTOR('',#7618,1.);
#2184=VECTOR('',#7631,0.25);
#2185=VECTOR('',#7644,0.4);
#2186=VECTOR('',#7649,0.425);
#2187=VECTOR('',#7654,0.41);
#2188=VECTOR('',#7663,0.26);
#2189=VECTOR('',#7666,0.25);
#2509=CIRCLE('',#6300,0.25);
#2510=CIRCLE('',#6301,0.24505);
#2511=CIRCLE('',#6303,0.25);
#2512=CIRCLE('',#6306,0.375);
#2513=CIRCLE('',#6308,0.425);
#2514=CIRCLE('',#6310,0.425);
#2515=CIRCLE('',#6312,0.395);
#2516=CIRCLE('',#6314,0.27);
#2517=CIRCLE('',#6316,0.24505);
#2862=VERTEX_POINT('',#9380);
#2863=VERTEX_POINT('',#9381);
#2864=VERTEX_POINT('',#9383);
#2865=VERTEX_POINT('',#9385);
#2866=VERTEX_POINT('',#9389);
#2867=VERTEX_POINT('',#9391);
#2868=VERTEX_POINT('',#9395);
#2869=VERTEX_POINT('',#9397);
#2870=VERTEX_POINT('',#9401);
#2871=VERTEX_POINT('',#9403);
#2872=VERTEX_POINT('',#9407);
#2873=VERTEX_POINT('',#9409);
#2874=VERTEX_POINT('',#9418);
#2875=VERTEX_POINT('',#9420);
#2876=VERTEX_POINT('',#9423);
#2877=VERTEX_POINT('',#9428);
#2878=VERTEX_POINT('',#9431);
#2879=VERTEX_POINT('',#9435);
#2880=VERTEX_POINT('',#9439);
#2881=VERTEX_POINT('',#9443);
#2882=VERTEX_POINT('',#9446);
#3468=EDGE_CURVE('',#2862,#2863,#1748,.T.);
#3469=EDGE_CURVE('',#2863,#2864,#1749,.T.);
#3470=EDGE_CURVE('',#2864,#2865,#1750,.T.);
#3471=EDGE_CURVE('',#2862,#2865,#1751,.T.);
#3472=EDGE_CURVE('',#2863,#2866,#1752,.T.);
#3473=EDGE_CURVE('',#2866,#2867,#1753,.T.);
#3474=EDGE_CURVE('',#2867,#2864,#1754,.T.);
#3475=EDGE_CURVE('',#2866,#2868,#1755,.T.);
#3476=EDGE_CURVE('',#2868,#2869,#1756,.T.);
#3477=EDGE_CURVE('',#2869,#2867,#1757,.T.);
#3478=EDGE_CURVE('',#2868,#2870,#1758,.T.);
#3479=EDGE_CURVE('',#2870,#2871,#1759,.T.);
#3480=EDGE_CURVE('',#2871,#2869,#1760,.T.);
#3481=EDGE_CURVE('',#2870,#2872,#1761,.T.);
#3482=EDGE_CURVE('',#2872,#2873,#1762,.T.);
#3483=EDGE_CURVE('',#2873,#2871,#1763,.T.);
#3484=EDGE_CURVE('',#2872,#2862,#1764,.T.);
#3485=EDGE_CURVE('',#2865,#2873,#1765,.T.);
#3486=EDGE_CURVE('',#2874,#2874,#2509,.T.);
#3487=EDGE_CURVE('',#2875,#2875,#2510,.T.);
#3488=EDGE_CURVE('',#2874,#2876,#1766,.T.);
#3489=EDGE_CURVE('',#2876,#2876,#2511,.T.);
#3490=EDGE_CURVE('',#2877,#2877,#2512,.T.);
#3491=EDGE_CURVE('',#2878,#2878,#2513,.T.);
#3492=EDGE_CURVE('',#2878,#2877,#1767,.T.);
#3493=EDGE_CURVE('',#2879,#2879,#2514,.T.);
#3494=EDGE_CURVE('',#2879,#2878,#1768,.T.);
#3495=EDGE_CURVE('',#2880,#2880,#2515,.T.);
#3496=EDGE_CURVE('',#2880,#2879,#1769,.T.);
#3497=EDGE_CURVE('',#2881,#2881,#2516,.T.);
#3498=EDGE_CURVE('',#2882,#2882,#2517,.F.);
#3499=EDGE_CURVE('',#2882,#2881,#1770,.T.);
#3500=EDGE_CURVE('',#2875,#2882,#1771,.T.);
#4603=ORIENTED_EDGE('',*,*,#3468,.T.);
#4604=ORIENTED_EDGE('',*,*,#3469,.T.);
#4605=ORIENTED_EDGE('',*,*,#3470,.T.);
#4606=ORIENTED_EDGE('',*,*,#3471,.F.);
#4607=ORIENTED_EDGE('',*,*,#3472,.T.);
#4608=ORIENTED_EDGE('',*,*,#3473,.T.);
#4609=ORIENTED_EDGE('',*,*,#3474,.T.);
#4610=ORIENTED_EDGE('',*,*,#3469,.F.);
#4611=ORIENTED_EDGE('',*,*,#3475,.T.);
#4612=ORIENTED_EDGE('',*,*,#3476,.T.);
#4613=ORIENTED_EDGE('',*,*,#3477,.T.);
#4614=ORIENTED_EDGE('',*,*,#3473,.F.);
#4615=ORIENTED_EDGE('',*,*,#3478,.T.);
#4616=ORIENTED_EDGE('',*,*,#3479,.T.);
#4617=ORIENTED_EDGE('',*,*,#3480,.T.);
#4618=ORIENTED_EDGE('',*,*,#3476,.F.);
#4619=ORIENTED_EDGE('',*,*,#3481,.T.);
#4620=ORIENTED_EDGE('',*,*,#3482,.T.);
#4621=ORIENTED_EDGE('',*,*,#3483,.T.);
#4622=ORIENTED_EDGE('',*,*,#3479,.F.);
#4623=ORIENTED_EDGE('',*,*,#3484,.T.);
#4624=ORIENTED_EDGE('',*,*,#3471,.T.);
#4625=ORIENTED_EDGE('',*,*,#3485,.T.);
#4626=ORIENTED_EDGE('',*,*,#3482,.F.);
#4627=ORIENTED_EDGE('',*,*,#3484,.F.);
#4628=ORIENTED_EDGE('',*,*,#3481,.F.);
#4629=ORIENTED_EDGE('',*,*,#3478,.F.);
#4630=ORIENTED_EDGE('',*,*,#3475,.F.);
#4631=ORIENTED_EDGE('',*,*,#3472,.F.);
#4632=ORIENTED_EDGE('',*,*,#3468,.F.);
#4633=ORIENTED_EDGE('',*,*,#3485,.F.);
#4634=ORIENTED_EDGE('',*,*,#3470,.F.);
#4635=ORIENTED_EDGE('',*,*,#3474,.F.);
#4636=ORIENTED_EDGE('',*,*,#3477,.F.);
#4637=ORIENTED_EDGE('',*,*,#3480,.F.);
#4638=ORIENTED_EDGE('',*,*,#3483,.F.);
#4639=ORIENTED_EDGE('',*,*,#3486,.T.);
#4640=ORIENTED_EDGE('',*,*,#3487,.F.);
#4641=ORIENTED_EDGE('',*,*,#3486,.F.);
#4642=ORIENTED_EDGE('',*,*,#3488,.T.);
#4643=ORIENTED_EDGE('',*,*,#3489,.T.);
#4644=ORIENTED_EDGE('',*,*,#3488,.F.);
#4645=ORIENTED_EDGE('',*,*,#3489,.F.);
#4646=ORIENTED_EDGE('',*,*,#3490,.F.);
#4647=ORIENTED_EDGE('',*,*,#3491,.F.);
#4648=ORIENTED_EDGE('',*,*,#3492,.T.);
#4649=ORIENTED_EDGE('',*,*,#3490,.T.);
#4650=ORIENTED_EDGE('',*,*,#3492,.F.);
#4651=ORIENTED_EDGE('',*,*,#3493,.F.);
#4652=ORIENTED_EDGE('',*,*,#3494,.T.);
#4653=ORIENTED_EDGE('',*,*,#3491,.T.);
#4654=ORIENTED_EDGE('',*,*,#3494,.F.);
#4655=ORIENTED_EDGE('',*,*,#3495,.F.);
#4656=ORIENTED_EDGE('',*,*,#3496,.T.);
#4657=ORIENTED_EDGE('',*,*,#3493,.T.);
#4658=ORIENTED_EDGE('',*,*,#3496,.F.);
#4659=ORIENTED_EDGE('',*,*,#3495,.T.);
#4660=ORIENTED_EDGE('',*,*,#3497,.F.);
#4661=ORIENTED_EDGE('',*,*,#3498,.F.);
#4662=ORIENTED_EDGE('',*,*,#3499,.T.);
#4663=ORIENTED_EDGE('',*,*,#3497,.T.);
#4664=ORIENTED_EDGE('',*,*,#3499,.F.);
#4665=ORIENTED_EDGE('',*,*,#3487,.T.);
#4666=ORIENTED_EDGE('',*,*,#3500,.T.);
#4667=ORIENTED_EDGE('',*,*,#3498,.T.);
#4668=ORIENTED_EDGE('',*,*,#3500,.F.);
#5226=CYLINDRICAL_SURFACE('',#6302,0.25);
#5227=CYLINDRICAL_SURFACE('',#6309,0.425);
#5228=CYLINDRICAL_SURFACE('',#6317,0.24505);
#5441=ADVANCED_FACE('',(#941),#646,.F.);
#5442=ADVANCED_FACE('',(#942),#647,.F.);
#5443=ADVANCED_FACE('',(#943),#648,.F.);
#5444=ADVANCED_FACE('',(#944),#649,.F.);
#5445=ADVANCED_FACE('',(#945),#650,.F.);
#5446=ADVANCED_FACE('',(#946),#651,.F.);
#5447=ADVANCED_FACE('',(#947),#652,.F.);
#5448=ADVANCED_FACE('',(#948),#653,.F.);
#5449=ADVANCED_FACE('',(#949,#513),#654,.T.);
#5450=ADVANCED_FACE('',(#950),#5226,.T.);
#5451=ADVANCED_FACE('',(#951),#655,.F.);
#5452=ADVANCED_FACE('',(#952),#656,.T.);
#5453=ADVANCED_FACE('',(#953),#266,.T.);
#5454=ADVANCED_FACE('',(#954),#5227,.T.);
#5455=ADVANCED_FACE('',(#955),#267,.T.);
#5456=ADVANCED_FACE('',(#956,#514),#657,.T.);
#5457=ADVANCED_FACE('',(#957),#268,.T.);
#5458=ADVANCED_FACE('',(#958),#5228,.T.);
#5592=CLOSED_SHELL('',(#5441,#5442,#5443,#5444,#5445,#5446,#5447,#5448));
#5593=CLOSED_SHELL('',(#5449,#5450,#5451,#5452,#5453,#5454,#5455,#5456,
#5457,#5458));
#6290=AXIS2_PLACEMENT_3D('',#9378,#7587,#7588);
#6291=AXIS2_PLACEMENT_3D('',#9379,#7589,#7590);
#6292=AXIS2_PLACEMENT_3D('',#9388,#7595,#7596);
#6293=AXIS2_PLACEMENT_3D('',#9394,#7600,#7601);
#6294=AXIS2_PLACEMENT_3D('',#9400,#7605,#7606);
#6295=AXIS2_PLACEMENT_3D('',#9406,#7610,#7611);
#6296=AXIS2_PLACEMENT_3D('',#9412,#7615,#7616);
#6297=AXIS2_PLACEMENT_3D('',#9415,#7619,#7620);
#6298=AXIS2_PLACEMENT_3D('',#9416,#7621,#7622);
#6299=AXIS2_PLACEMENT_3D('',#9417,#7623,#7624);
#6300=AXIS2_PLACEMENT_3D('',#9419,#7625,#7626);
#6301=AXIS2_PLACEMENT_3D('',#9421,#7627,#7628);
#6302=AXIS2_PLACEMENT_3D('',#9422,#7629,#7630);
#6303=AXIS2_PLACEMENT_3D('',#9425,#7632,#7633);
#6304=AXIS2_PLACEMENT_3D('',#9426,#7634,#7635);
#6305=AXIS2_PLACEMENT_3D('',#9427,#7636,#7637);
#6306=AXIS2_PLACEMENT_3D('',#9429,#7638,#7639);
#6307=AXIS2_PLACEMENT_3D('',#9430,#7640,#7641);
#6308=AXIS2_PLACEMENT_3D('',#9432,#7642,#7643);
#6309=AXIS2_PLACEMENT_3D('',#9434,#7645,#7646);
#6310=AXIS2_PLACEMENT_3D('',#9436,#7647,#7648);
#6311=AXIS2_PLACEMENT_3D('',#9438,#7650,#7651);
#6312=AXIS2_PLACEMENT_3D('',#9440,#7652,#7653);
#6313=AXIS2_PLACEMENT_3D('',#9442,#7655,#7656);
#6314=AXIS2_PLACEMENT_3D('',#9444,#7657,#7658);
#6315=AXIS2_PLACEMENT_3D('',#9445,#7659,#7660);
#6316=AXIS2_PLACEMENT_3D('',#9447,#7661,#7662);
#6317=AXIS2_PLACEMENT_3D('',#9449,#7664,#7665);
#7587=DIRECTION('axis',(0.,0.,1.));
#7588=DIRECTION('refdir',(1.,0.,0.));
#7589=DIRECTION('center_axis',(0.866025403784439,0.,-0.5));
#7590=DIRECTION('ref_axis',(0.5,0.,0.866025403784439));
#7591=DIRECTION('',(-0.5,0.,-0.866025403784439));
#7592=DIRECTION('',(0.,-1.,0.));
#7593=DIRECTION('',(0.5,0.,0.866025403784439));
#7594=DIRECTION('',(0.,-1.,0.));
#7595=DIRECTION('center_axis',(1.20185167898973E-16,0.,-1.));
#7596=DIRECTION('ref_axis',(1.,0.,1.20185167898973E-16));
#7597=DIRECTION('',(-1.,0.,-1.20185167898973E-16));
#7598=DIRECTION('',(0.,-1.,0.));
#7599=DIRECTION('',(1.,0.,1.20185167898973E-16));
#7600=DIRECTION('center_axis',(-0.866025403784439,0.,-0.5));
#7601=DIRECTION('ref_axis',(0.5,0.,-0.866025403784439));
#7602=DIRECTION('',(-0.5,0.,0.866025403784439));
#7603=DIRECTION('',(0.,-1.,0.));
#7604=DIRECTION('',(0.5,0.,-0.866025403784439));
#7605=DIRECTION('center_axis',(-0.866025403784439,0.,0.5));
#7606=DIRECTION('ref_axis',(-0.5,0.,-0.866025403784439));
#7607=DIRECTION('',(0.5,0.,0.866025403784439));
#7608=DIRECTION('',(0.,-1.,0.));
#7609=DIRECTION('',(-0.5,0.,-0.866025403784439));
#7610=DIRECTION('center_axis',(-2.40370335797945E-16,0.,1.));
#7611=DIRECTION('ref_axis',(-1.,0.,-2.40370335797945E-16));
#7612=DIRECTION('',(1.,0.,2.40370335797945E-16));
#7613=DIRECTION('',(0.,-1.,0.));
#7614=DIRECTION('',(-1.,0.,-2.40370335797945E-16));
#7615=DIRECTION('center_axis',(0.866025403784439,0.,0.5));
#7616=DIRECTION('ref_axis',(-0.5,0.,0.866025403784439));
#7617=DIRECTION('',(0.5,0.,-0.866025403784439));
#7618=DIRECTION('',(-0.5,0.,0.866025403784439));
#7619=DIRECTION('center_axis',(0.,1.,0.));
#7620=DIRECTION('ref_axis',(1.,0.,0.));
#7621=DIRECTION('center_axis',(0.,-1.,0.));
#7622=DIRECTION('ref_axis',(0.,0.,-1.));
#7623=DIRECTION('center_axis',(0.,1.,0.));
#7624=DIRECTION('ref_axis',(1.,0.,0.));
#7625=DIRECTION('center_axis',(0.,1.,0.));
#7626=DIRECTION('ref_axis',(1.,0.,0.));
#7627=DIRECTION('center_axis',(0.,1.,0.));
#7628=DIRECTION('ref_axis',(1.,0.,0.));
#7629=DIRECTION('center_axis',(0.,1.,0.));
#7630=DIRECTION('ref_axis',(1.,0.,0.));
#7631=DIRECTION('',(0.,-1.,0.));
#7632=DIRECTION('center_axis',(0.,1.,0.));
#7633=DIRECTION('ref_axis',(1.,0.,0.));
#7634=DIRECTION('center_axis',(0.,1.,0.));
#7635=DIRECTION('ref_axis',(1.,0.,0.));
#7636=DIRECTION('center_axis',(0.,1.,0.));
#7637=DIRECTION('ref_axis',(0.,0.,1.));
#7638=DIRECTION('center_axis',(0.,-1.,0.));
#7639=DIRECTION('ref_axis',(1.,0.,0.));
#7640=DIRECTION('center_axis',(0.,-1.,0.));
#7641=DIRECTION('ref_axis',(1.,0.,0.));
#7642=DIRECTION('center_axis',(0.,-1.,0.));
#7643=DIRECTION('ref_axis',(1.,0.,0.));
#7644=DIRECTION('',(0.707106781186548,0.707106781186547,8.65956056235493E-17));
#7645=DIRECTION('center_axis',(0.,-1.,0.));
#7646=DIRECTION('ref_axis',(1.,0.,0.));
#7647=DIRECTION('center_axis',(0.,-1.,0.));
#7648=DIRECTION('ref_axis',(1.,0.,0.));
#7649=DIRECTION('',(0.,1.,0.));
#7650=DIRECTION('center_axis',(0.,1.,0.));
#7651=DIRECTION('ref_axis',(1.,0.,0.));
#7652=DIRECTION('center_axis',(0.,-1.,0.));
#7653=DIRECTION('ref_axis',(1.,0.,0.));
#7654=DIRECTION('',(-0.707106781186547,0.707106781186548,-8.65956056235493E-17));
#7655=DIRECTION('center_axis',(0.,-1.,0.));
#7656=DIRECTION('ref_axis',(0.,0.,-1.));
#7657=DIRECTION('center_axis',(0.,-1.,0.));
#7658=DIRECTION('ref_axis',(1.,0.,0.));
#7659=DIRECTION('center_axis',(0.,1.,0.));
#7660=DIRECTION('ref_axis',(1.,0.,0.));
#7661=DIRECTION('center_axis',(0.,1.,0.));
#7662=DIRECTION('ref_axis',(1.,0.,0.));
#7663=DIRECTION('',(-0.447213595499958,0.894427190999916,-5.47678698264203E-17));
#7664=DIRECTION('center_axis',(0.,-1.,0.));
#7665=DIRECTION('ref_axis',(1.,0.,0.));
#7666=DIRECTION('',(0.,1.,0.));
#9378=CARTESIAN_POINT('',(0.,0.,0.));
#9379=CARTESIAN_POINT('Origin',(0.115470053837925,-0.5,-0.2));
#9380=CARTESIAN_POINT('',(0.23094010767585,-0.5,0.));
#9381=CARTESIAN_POINT('',(0.115470053837925,-0.5,-0.2));
#9382=CARTESIAN_POINT('',(0.23094010767585,-0.5,0.));
#9383=CARTESIAN_POINT('',(0.115470053837925,-0.8,-0.2));
#9384=CARTESIAN_POINT('',(0.115470053837925,-0.5,-0.2));
#9385=CARTESIAN_POINT('',(0.23094010767585,-0.8,0.));
#9386=CARTESIAN_POINT('',(0.23094010767585,-0.8,0.));
#9387=CARTESIAN_POINT('',(0.23094010767585,-0.5,0.));
#9388=CARTESIAN_POINT('Origin',(-0.115470053837925,-0.5,-0.2));
#9389=CARTESIAN_POINT('',(-0.115470053837925,-0.5,-0.2));
#9390=CARTESIAN_POINT('',(0.115470053837925,-0.5,-0.2));
#9391=CARTESIAN_POINT('',(-0.115470053837925,-0.8,-0.2));
#9392=CARTESIAN_POINT('',(-0.115470053837925,-0.5,-0.2));
#9393=CARTESIAN_POINT('',(0.115470053837925,-0.8,-0.2));
#9394=CARTESIAN_POINT('Origin',(-0.23094010767585,-0.5,-2.77555756156289E-17));
#9395=CARTESIAN_POINT('',(-0.23094010767585,-0.5,-2.82820063659975E-17));
#9396=CARTESIAN_POINT('',(-0.115470053837925,-0.5,-0.2));
#9397=CARTESIAN_POINT('',(-0.23094010767585,-0.8,-2.77555756156289E-17));
#9398=CARTESIAN_POINT('',(-0.23094010767585,-0.5,-2.82820063659975E-17));
#9399=CARTESIAN_POINT('',(-0.115470053837925,-0.8,-0.2));
#9400=CARTESIAN_POINT('Origin',(-0.115470053837925,-0.5,0.2));
#9401=CARTESIAN_POINT('',(-0.115470053837925,-0.5,0.2));
#9402=CARTESIAN_POINT('',(-0.23094010767585,-0.5,-2.82820063659975E-17));
#9403=CARTESIAN_POINT('',(-0.115470053837925,-0.8,0.2));
#9404=CARTESIAN_POINT('',(-0.115470053837925,-0.5,0.2));
#9405=CARTESIAN_POINT('',(-0.23094010767585,-0.8,-2.82820063659975E-17));
#9406=CARTESIAN_POINT('Origin',(0.115470053837925,-0.5,0.2));
#9407=CARTESIAN_POINT('',(0.115470053837925,-0.5,0.2));
#9408=CARTESIAN_POINT('',(-0.115470053837925,-0.5,0.2));
#9409=CARTESIAN_POINT('',(0.115470053837925,-0.8,0.2));
#9410=CARTESIAN_POINT('',(0.115470053837925,-0.5,0.2));
#9411=CARTESIAN_POINT('',(-0.115470053837925,-0.8,0.2));
#9412=CARTESIAN_POINT('Origin',(0.23094010767585,-0.5,0.));
#9413=CARTESIAN_POINT('',(0.115470053837925,-0.5,0.2));
#9414=CARTESIAN_POINT('',(0.115470053837925,-0.8,0.2));
#9415=CARTESIAN_POINT('Origin',(0.,-0.5,0.));
#9416=CARTESIAN_POINT('Origin',(0.,-0.8,0.));
#9417=CARTESIAN_POINT('Origin',(0.,-1.9,0.));
#9418=CARTESIAN_POINT('',(-0.25,-1.9,3.06161699786838E-17));
#9419=CARTESIAN_POINT('Origin',(0.,-1.9,0.));
#9420=CARTESIAN_POINT('',(-0.24505,-1.9,3.00099698131059E-17));
#9421=CARTESIAN_POINT('Origin',(0.,-1.9,0.));
#9422=CARTESIAN_POINT('Origin',(0.,-7.,0.));
#9423=CARTESIAN_POINT('',(-0.25,-7.,3.06161699786838E-17));
#9424=CARTESIAN_POINT('',(-0.25,-7.,3.06161699786838E-17));
#9425=CARTESIAN_POINT('Origin',(0.,-7.,0.));
#9426=CARTESIAN_POINT('Origin',(0.,-7.,0.));
#9427=CARTESIAN_POINT('Origin',(0.375,0.5,0.));
#9428=CARTESIAN_POINT('',(-0.375,0.5,-4.59242549680257E-17));
#9429=CARTESIAN_POINT('Origin',(0.,0.5,0.));
#9430=CARTESIAN_POINT('Origin',(0.,0.475,0.));
#9431=CARTESIAN_POINT('',(-0.425,0.45,-5.20474889637625E-17));
#9432=CARTESIAN_POINT('Origin',(0.,0.45,0.));
#9433=CARTESIAN_POINT('',(-0.4,0.475,-4.89858719658941E-17));
#9434=CARTESIAN_POINT('Origin',(0.,0.24,0.));
#9435=CARTESIAN_POINT('',(-0.425,0.0299999999999998,-5.20474889637625E-17));
#9436=CARTESIAN_POINT('Origin',(0.,0.0299999999999998,0.));
#9437=CARTESIAN_POINT('',(-0.425,0.24,-5.20474889637625E-17));
#9438=CARTESIAN_POINT('Origin',(0.,0.0150000000000001,0.));
#9439=CARTESIAN_POINT('',(-0.395,4.85722573273506E-17,-4.83735485663204E-17));
#9440=CARTESIAN_POINT('Origin',(0.,0.,0.));
#9441=CARTESIAN_POINT('',(-0.41,0.0150000000000001,-5.02105187650415E-17));
#9442=CARTESIAN_POINT('Origin',(0.27,0.,0.));
#9443=CARTESIAN_POINT('',(-0.27,0.,-3.30654635769785E-17));
#9444=CARTESIAN_POINT('Origin',(0.,0.,0.));
#9445=CARTESIAN_POINT('Origin',(0.,-0.02,0.));
#9446=CARTESIAN_POINT('',(-0.24505,-0.0498999999999999,3.00099698131059E-17));
#9447=CARTESIAN_POINT('Origin',(0.,-0.0498999999999999,0.));
#9448=CARTESIAN_POINT('',(-0.26,-0.02,-3.18408167778312E-17));
#9449=CARTESIAN_POINT('Origin',(0.,-0.995,0.));
#9450=CARTESIAN_POINT('',(-0.24505,-0.995,-3.00099698131059E-17));
#10074=UNCERTAINTY_MEASURE_WITH_UNIT(LENGTH_MEASURE(0.001),#10120,
'DISTANCE_ACCURACY_VALUE',
'Maximum model space distance between geometric entities at asserted c
onnectivities');
#10088=UNCERTAINTY_MEASURE_WITH_UNIT(LENGTH_MEASURE(0.001),#10120,
'DISTANCE_ACCURACY_VALUE',
'Maximum model space distance between geometric entities at asserted c
onnectivities');
#10105=(
GEOMETRIC_REPRESENTATION_CONTEXT(3)
GLOBAL_UNCERTAINTY_ASSIGNED_CONTEXT((#10074))
GLOBAL_UNIT_ASSIGNED_CONTEXT((#10120,#10122,#10123))
REPRESENTATION_CONTEXT('','3D')
);
#10119=(
GEOMETRIC_REPRESENTATION_CONTEXT(3)
GLOBAL_UNCERTAINTY_ASSIGNED_CONTEXT((#10088))
GLOBAL_UNIT_ASSIGNED_CONTEXT((#10120,#10122,#10123))
REPRESENTATION_CONTEXT('','3D')
);
#10120=(
LENGTH_UNIT()
NAMED_UNIT(*)
SI_UNIT(.CENTI.,.METRE.)
);
#10122=(
NAMED_UNIT(*)
PLANE_ANGLE_UNIT()
SI_UNIT($,.RADIAN.)
);
#10123=(
NAMED_UNIT(*)
SI_UNIT($,.STERADIAN.)
SOLID_ANGLE_UNIT()
);
#10140=SHAPE_DEFINITION_REPRESENTATION(#10170,#10256);
#10170=PRODUCT_DEFINITION_SHAPE('',$,#10287);
#10256=SHAPE_REPRESENTATION('',(#6290),#10105);
#10270=PRODUCT_DEFINITION_CONTEXT('part definition',#10362,'design');
#10287=PRODUCT_DEFINITION('M5x70 body screw','M5x70 body screw',#10317,
#10270);
#10317=PRODUCT_DEFINITION_FORMATION('',$,#10380);
#10362=APPLICATION_CONTEXT(
'Core Data for Automotive Mechanical Design Process');
#10363=PRODUCT_CONTEXT('part definition',#10362,'mechanical');
#10380=PRODUCT('M5x70 body screw','M5x70 body screw','M5x70 body screw',
(#10363));
#10471=COLOUR_RGB('Black',0.12,0.14,0.17);
#10472=FILL_AREA_STYLE_COLOUR('',#10471);
#10473=FILL_AREA_STYLE('',(#10472));
#10474=SURFACE_STYLE_FILL_AREA(#10473);
#10475=SURFACE_SIDE_STYLE('',(#10474));
#10476=SURFACE_STYLE_USAGE(.BOTH.,#10475);
#10477=PRESENTATION_STYLE_ASSIGNMENT((#10476));
ENDSEC;
END-ISO-10303-21;
